ISO-10303-21;
HEADER;
FILE_DESCRIPTION (('STEP AP214'),
    '1' );
FILE_NAME ('Slotted Screw.step',
    '2026-10-06T13:23:30',
    ( '' ),
    ( '' ),
    'SwSTEP 2.0',
    'SolidWorks 2020',
    '' );
FILE_SCHEMA (( 'AUTOMOTIVE_DESIGN' ));
ENDSEC;

DATA;
#131=FACE_OUTER_BOUND ( 'NONE', #19542, .T. ) ;
#261=CARTESIAN_POINT ( 'NONE',  ( -35.47299999999999898, 14.00000000000000000, -143.5552959529999839 ) ) ;
#395=CARTESIAN_POINT ( 'NONE',  ( -35.07300000000000040, 14.00000000000000000, -144.5552959529999839 ) ) ;
#610=EDGE_LOOP ( 'NONE', ( #15097, #4156, #2830, #8303 ) ) ;
#656=FACE_OUTER_BOUND ( 'NONE', #610, .T. ) ;
#736=CARTESIAN_POINT ( 'NONE',  ( -35.47299999999999898, 14.00000000000000000, -144.0552959529999839 ) ) ;
#756=CIRCLE ( 'NONE', #18597, 2.600000000000000089 ) ;
#913=ORIENTED_EDGE ( 'NONE', *, *, #20692, .F. ) ;
#915=VERTEX_POINT ( 'NONE', #10353 ) ;
#1098=ORIENTED_EDGE ( 'NONE', *, *, #3445, .F. ) ;
#1149=AXIS2_PLACEMENT_3D ( 'NONE', #23405, #16268, #10529 ) ;
#1161=DIRECTION ( 'NONE',  ( 1.000000000000000000, 0.000000000000000000, 0.000000000000000000 ) ) ;
#1210=ADVANCED_FACE ( 'NONE', ( #656 ), #13255, .T. ) ;
#1336=CARTESIAN_POINT ( 'NONE',  ( -26.47299999999999898, 14.00000000000000000, -144.0552959529999839 ) ) ;
#1384=UNCERTAINTY_MEASURE_WITH_UNIT (LENGTH_MEASURE( 1.000000000000000082E-05 ), #11513, 'distance_accuracy_value', 'NONE');
#1453=CIRCLE ( 'NONE', #17009, 2.000000000000000000 ) ;
#1454=CARTESIAN_POINT ( 'NONE',  ( -34.97299999999999898, 11.80604359530000025, -145.2538597989999971 ) ) ;
#1529=CONICAL_SURFACE ( 'NONE', #3036, 2.000000000000003553, 0.7853981633970000820 ) ;
#1531=AXIS2_PLACEMENT_3D ( 'NONE', #18208, #9370, #16534 ) ;
#1557=ORIENTED_EDGE ( 'NONE', *, *, #10489, .T. ) ;
#1575=CARTESIAN_POINT ( 'NONE',  ( -34.47299999999999898, 14.00000000000000000, -144.0552959529999839 ) ) ;
#2339=DIRECTION ( 'NONE',  ( 1.000000000000000000, 2.602084704497994558E-17, -1.701177080612860179E-20 ) ) ;
#2399=CARTESIAN_POINT ( 'NONE',  ( -35.33948162989999986, 11.17737245070000185, -144.5552959529999839 ) ) ;
#2405=COLOUR_RGB ( '', 0.09019608, 0.27058824, 0.51372549) ;
#2464=CARTESIAN_POINT ( 'NONE',  ( -35.47299999999999898, 14.00000000000000000, -144.0552959529999839 ) ) ;
#2530=FACE_OUTER_BOUND ( 'NONE', #18422, .T. ) ;
#2574=DIRECTION ( 'NONE',  ( -2.602084704489999637E-17, 1.000000000000000000, 0.000000000000000000 ) ) ;
#2611=ORIENTED_EDGE ( 'NONE', *, *, #6655, .F. ) ;
#2626=CARTESIAN_POINT ( 'NONE',  ( -35.20609992760000040, 16.68710169819999933, -143.5552959529999839 ) ) ;
#2710=DIRECTION ( 'NONE',  ( 0.000000000000000000, -1.000000000000000000, 0.000000000000000000 ) ) ;
#2747=CARTESIAN_POINT ( 'NONE',  ( -35.33948162989999986, 11.17737245070000185, -143.5552959529999839 ) ) ;
#2768=LINE ( 'NONE', #1454, #11832 ) ;
#2830=ORIENTED_EDGE ( 'NONE', *, *, #8283, .T. ) ;
#2898=CARTESIAN_POINT ( 'NONE',  ( -34.47299999999999898, 15.75516512379999945, -143.0964448760000209 ) ) ;
#2937=DIRECTION ( 'NONE',  ( 1.000000000000000000, 2.602084704489999637E-17, -1.701177084980000217E-20 ) ) ;
#2939=AXIS2_PLACEMENT_3D ( 'NONE', #9169, #5385, #3358 ) ;
#3036=AXIS2_PLACEMENT_3D ( 'NONE', #17242, #14148, #8427 ) ;
#3049=AXIS2_PLACEMENT_3D ( 'NONE', #5771, #2339, #4341 ) ;
#3178=B_SPLINE_CURVE_WITH_KNOTS ( 'NONE', 3,
 ( #4292, #2626, #15814, #10332 ),
 .UNSPECIFIED., .F., .F.,
 ( 4, 4 ),
 ( 0.000000000000000000, 0.8059436278830001132 ),
 .UNSPECIFIED. ) ;
#3223=CARTESIAN_POINT ( 'NONE',  ( -34.97299999999999898, 16.19395640470000330, -142.8567321060000097 ) ) ;
#3272=ORIENTED_EDGE ( 'NONE', *, *, #20794, .T. ) ;
#3358=DIRECTION ( 'NONE',  ( 0.000000000000000000, 1.000000000000000000, 0.000000000000000000 ) ) ;
#3393=EDGE_LOOP ( 'NONE', ( #22080, #3272, #20503, #5083 ) ) ;
#3445=EDGE_CURVE ( 'NONE', #12978, #8318, #13053, .T. ) ;
#3460=DIRECTION ( 'NONE',  ( -1.000000000000000000, 0.000000000000000000, 0.000000000000000000 ) ) ;
#3491=( NAMED_UNIT ( * ) PLANE_ANGLE_UNIT ( ) SI_UNIT ( $, .RADIAN. ) );
#3574=FACE_OUTER_BOUND ( 'NONE', #21255, .T. ) ;
#3686=AXIS2_PLACEMENT_3D ( 'NONE', #11944, #8724, #16003 ) ;
#3741=DIRECTION ( 'NONE',  ( 0.000000000000000000, 1.000000000000000000, 0.000000000000000000 ) ) ;
#3776=SURFACE_STYLE_USAGE ( .BOTH. , #16850 ) ;
#3809=DIRECTION ( 'NONE',  ( -1.000000000000000000, 0.000000000000000000, 1.701177084980000217E-20 ) ) ;
#3832=LINE ( 'NONE', #261, #17726 ) ;
#3875=AXIS2_PLACEMENT_3D ( 'NONE', #17145, #22619, #18089 ) ;
#3939=CARTESIAN_POINT ( 'NONE',  ( -35.07300000000000040, 11.44852983560000048, -144.5552959529999839 ) ) ;
#4014=ORIENTED_EDGE ( 'NONE', *, *, #8927, .T. ) ;
#4114=STYLED_ITEM ( 'NONE', ( #5784 ), #20181 ) ;
#4156=ORIENTED_EDGE ( 'NONE', *, *, #7538, .T. ) ;
#4218=PRODUCT ( 'Slotted Screw', 'Slotted Screw', '', ( #22218 ) ) ;
#4290=CARTESIAN_POINT ( 'NONE',  ( -35.47299999999999898, 11.04196010839999964, -144.5552959529999839 ) ) ;
#4292=CARTESIAN_POINT ( 'NONE',  ( -35.07300000000000040, 16.55147016440000129, -143.5552959529999839 ) ) ;
#4324=ORIENTED_EDGE ( 'NONE', *, *, #19785, .T. ) ;
#4341=DIRECTION ( 'NONE',  ( 0.000000000000000000, 0.8775825618903703162, 0.4794255386042076128 ) ) ;
#4373=B_SPLINE_CURVE_WITH_KNOTS ( 'NONE', 3,
 ( #5165, #12414, #14334, #17911 ),
 .UNSPECIFIED., .F., .F.,
 ( 4, 4 ),
 ( 0.000000000000000000, 0.8059436278830001132 ),
 .UNSPECIFIED. ) ;
#4413=FACE_OUTER_BOUND ( 'NONE', #3393, .T. ) ;
#4590=CARTESIAN_POINT ( 'NONE',  ( 0.000000000000000000, 0.000000000000000000, 0.000000000000000000 ) ) ;
#4631=SURFACE_STYLE_USAGE ( .BOTH. , #8065 ) ;
#4733=CARTESIAN_POINT ( 'NONE',  ( -30.47299999999999898, 12.24483487620000055, -145.0141470300000037 ) ) ;
#4899=VERTEX_POINT ( 'NONE', #10333 ) ;
#4932=CARTESIAN_POINT ( 'NONE',  ( -35.07300000000000040, 14.00000000000000000, -143.5552959529999839 ) ) ;
#5008=LINE ( 'NONE', #3223, #11331 ) ;
#5025=AXIS2_PLACEMENT_3D ( 'NONE', #4590, #17084, #1161 ) ;
#5027=ORIENTED_EDGE ( 'NONE', *, *, #23478, .F. ) ;
#5083=ORIENTED_EDGE ( 'NONE', *, *, #7538, .F. ) ;
#5165=CARTESIAN_POINT ( 'NONE',  ( -35.07300000000000040, 16.55147016440000129, -144.5552959529999839 ) ) ;
#5320=FACE_OUTER_BOUND ( 'NONE', #17317, .T. ) ;
#5385=DIRECTION ( 'NONE',  ( 1.000000000000000000, 2.602084704489999637E-17, -1.701177084980000217E-20 ) ) ;
#5480=DIRECTION ( 'NONE',  ( 1.000000000000000000, 2.602084704489999637E-17, -1.701177084980000217E-20 ) ) ;
#5481=ORIENTED_EDGE ( 'NONE', *, *, #8283, .F. ) ;
#5576=ORIENTED_EDGE ( 'NONE', *, *, #19428, .T. ) ;
#5703=CARTESIAN_POINT ( 'NONE',  ( -35.47299999999999898, 11.04196010839999964, -144.5552959529999839 ) ) ;
#5760=DIRECTION ( 'NONE',  ( 1.000000000000000000, 2.602084704489999637E-17, -1.701177084980000217E-20 ) ) ;
#5770=DIRECTION ( 'NONE',  ( 0.000000000000000000, -1.000000000000000000, 0.000000000000000000 ) ) ;
#5771=CARTESIAN_POINT ( 'NONE',  ( -30.97299999999999898, 14.00000000000000000, -144.0552959529999839 ) ) ;
#5784=PRESENTATION_STYLE_ASSIGNMENT (( #3776 ) ) ;
#5896=( NAMED_UNIT ( * ) SI_UNIT ( $, .STERADIAN. ) SOLID_ANGLE_UNIT ( ) );
#5968=PLANE ( 'NONE',  #9926 ) ;
#5981=AXIS2_PLACEMENT_3D ( 'NONE', #12718, #17971, #6896 ) ;
#6190=ADVANCED_FACE ( 'NONE', ( #5320 ), #12326, .F. ) ;
#6211=PRODUCT_DEFINITION_FORMATION_WITH_SPECIFIED_SOURCE ( 'ANY', '', #4218, .NOT_KNOWN. ) ;
#6272=ORIENTED_EDGE ( 'NONE', *, *, #10212, .T. ) ;
#6476=CARTESIAN_POINT ( 'NONE',  ( -35.07300000000000040, 11.44852983560000048, -143.5552959529999839 ) ) ;
#6655=EDGE_CURVE ( 'NONE', #8318, #11000, #9548, .T. ) ;
#6731=CIRCLE ( 'NONE', #2939, 3.000000000000000888 ) ;
#6896=DIRECTION ( 'NONE',  ( 0.000000000000000000, 0.8775825618903703162, 0.4794255386042076128 ) ) ;
#7113=CARTESIAN_POINT ( 'NONE',  ( -35.07300000000000040, 14.00000000000000000, -144.0552959529999839 ) ) ;
#7169=ORIENTED_EDGE ( 'NONE', *, *, #9488, .T. ) ;
#7205=VERTEX_POINT ( 'NONE', #20830 ) ;
#7236=DIRECTION ( 'NONE',  ( 0.000000000000000000, -1.000000000000000000, 0.000000000000000000 ) ) ;
#7304=ORIENTED_EDGE ( 'NONE', *, *, #14180, .F. ) ;
#7323=ORIENTED_EDGE ( 'NONE', *, *, #14180, .T. ) ;
#7446=PLANE ( 'NONE',  #12201 ) ;
#7485=ORIENTED_EDGE ( 'NONE', *, *, #14647, .T. ) ;
#7538=EDGE_CURVE ( 'NONE', #7205, #22524, #15684, .T. ) ;
#7599=AXIS2_PLACEMENT_3D ( 'NONE', #7113, #8765, #7236 ) ;
#7679=FACE_OUTER_BOUND ( 'NONE', #10202, .T. ) ;
#7688=SHAPE_DEFINITION_REPRESENTATION ( #9516, #14082 ) ;
#8065=SURFACE_SIDE_STYLE ('',( #20939 ) ) ;
#8225=ORIENTED_EDGE ( 'NONE', *, *, #19428, .F. ) ;
#8283=EDGE_CURVE ( 'NONE', #22524, #21589, #12524, .T. ) ;
#8303=ORIENTED_EDGE ( 'NONE', *, *, #20794, .F. ) ;
#8318=VERTEX_POINT ( 'NONE', #5703 ) ;
#8427=DIRECTION ( 'NONE',  ( 0.000000000000000000, 0.8775825618903703162, 0.4794255386042076128 ) ) ;
#8435=CARTESIAN_POINT ( 'NONE',  ( -35.47299999999999898, 11.04196010839999964, -143.5552959529999839 ) ) ;
#8443=ORIENTED_EDGE ( 'NONE', *, *, #18529, .T. ) ;
#8477=VERTEX_POINT ( 'NONE', #18895 ) ;
#8561=DIRECTION ( 'NONE',  ( -0.7071067811866730279, -0.6205445805637129775, -0.3390050494208429743 ) ) ;
#8669=LINE ( 'NONE', #9146, #9040 ) ;
#8724=DIRECTION ( 'NONE',  ( 1.000000000000000000, 2.602084704489999637E-17, -1.701177084980000217E-20 ) ) ;
#8765=DIRECTION ( 'NONE',  ( 1.000000000000000000, 2.602084704489999637E-17, -1.701177084980000217E-20 ) ) ;
#8894=ORIENTED_EDGE ( 'NONE', *, *, #3445, .T. ) ;
#8927=EDGE_CURVE ( 'NONE', #15926, #23345, #15968, .T. ) ;
#9017=DIRECTION ( 'NONE',  ( 1.000000000000000000, 2.602084704489999637E-17, -1.701177084980000217E-20 ) ) ;
#9040=VECTOR ( 'NONE', #3460, 1000.000000000000000 ) ;
#9063=AXIS2_PLACEMENT_3D ( 'NONE', #1336, #13823, #17737 ) ;
#9113=ORIENTED_EDGE ( 'NONE', *, *, #14325, .F. ) ;
#9146=CARTESIAN_POINT ( 'NONE',  ( -30.47299999999999898, 15.75516512379999945, -143.0964448760000209 ) ) ;
#9169=CARTESIAN_POINT ( 'NONE',  ( -35.47299999999999898, 14.00000000000000000, -144.0552959529999839 ) ) ;
#9370=DIRECTION ( 'NONE',  ( 1.000000000000000000, 2.602084704489999637E-17, -1.701177084980000217E-20 ) ) ;
#9413=MECHANICAL_DESIGN_GEOMETRIC_PRESENTATION_REPRESENTATION('',(#4114),#18171);
#9488=EDGE_CURVE ( 'NONE', #915, #7205, #16690, .T. ) ;
#9516=PRODUCT_DEFINITION_SHAPE ( 'NONE', 'NONE',  #10209 ) ;
#9528=AXIS2_PLACEMENT_3D ( 'NONE', #2464, #14079, #2574 ) ;
#9548=LINE ( 'NONE', #11207, #23451 ) ;
#9871=CYLINDRICAL_SURFACE ( 'NONE', #3875, 2.000000000000003553 ) ;
#9877=DIRECTION ( 'NONE',  ( 1.701177084980000217E-20, -2.602084704489999637E-17, 1.000000000000000000 ) ) ;
#9916=ADVANCED_FACE ( 'NONE', ( #11876 ), #1529, .T. ) ;
#9926=AXIS2_PLACEMENT_3D ( 'NONE', #395, #9877, #13458 ) ;
#9960=ORIENTED_EDGE ( 'NONE', *, *, #17254, .F. ) ;
#10199=SHAPE_REPRESENTATION_RELATIONSHIP ( 'NONE' , 'NONE' ,  #14082, #23143 ) ;
#10202=EDGE_LOOP ( 'NONE', ( #11869, #12356, #5027 ) ) ;
#10209=PRODUCT_DEFINITION ( 'UNKNOWN', '', #6211, #17316 ) ;
#10211=CARTESIAN_POINT ( 'NONE',  ( -35.20609992760000040, 11.31289830180000067, -143.5552959529999839 ) ) ;
#10212=EDGE_CURVE ( 'NONE', #10651, #12978, #756, .T. ) ;
#10332=CARTESIAN_POINT ( 'NONE',  ( -35.47299999999999898, 16.95803989150000035, -143.5552959529999839 ) ) ;
#10333=CARTESIAN_POINT ( 'NONE',  ( -35.47299999999999898, 16.63274768570000006, -142.6170193369999879 ) ) ;
#10353=CARTESIAN_POINT ( 'NONE',  ( -26.47299999999999898, 15.75516512379999945, -143.0964448760000209 ) ) ;
#10356=ORIENTED_EDGE ( 'NONE', *, *, #17254, .T. ) ;
#10424=ORIENTED_EDGE ( 'NONE', *, *, #16680, .F. ) ;
#10453=DIRECTION ( 'NONE',  ( -0.7071067811866730279, 0.6205445805637129775, 0.3390050494208429743 ) ) ;
#10489=EDGE_CURVE ( 'NONE', #15926, #12978, #14823, .T. ) ;
#10529=DIRECTION ( 'NONE',  ( -2.602084704489999637E-17, 1.000000000000000000, 0.000000000000000000 ) ) ;
#10633=UNCERTAINTY_MEASURE_WITH_UNIT (LENGTH_MEASURE( 1.000000000000000082E-05 ), #16607, 'distance_accuracy_value', 'NONE');
#10651=VERTEX_POINT ( 'NONE', #6476 ) ;
#10662=ORIENTED_EDGE ( 'NONE', *, *, #23478, .T. ) ;
#10672=ORIENTED_EDGE ( 'NONE', *, *, #10489, .F. ) ;
#10681=EDGE_CURVE ( 'NONE', #23345, #10651, #19324, .T. ) ;
#10730=( GEOMETRIC_REPRESENTATION_CONTEXT ( 3 ) GLOBAL_UNCERTAINTY_ASSIGNED_CONTEXT ( ( #1384 ) ) GLOBAL_UNIT_ASSIGNED_CONTEXT ( ( #11513, #3491, #20694 ) ) REPRESENTATION_CONTEXT ( 'NONE', 'WORKASPACE' ) );
#11000=VERTEX_POINT ( 'NONE', #22577 ) ;
#11059=CLOSED_SHELL ( 'NONE', ( #17619, #6190, #12682, #9916, #19715, #22499, #22321, #18990, #1210, #22927 ) ) ;
#11207=CARTESIAN_POINT ( 'NONE',  ( -35.47299999999999898, 14.00000000000000000, -144.5552959529999839 ) ) ;
#11331=VECTOR ( 'NONE', #10453, 1000.000000000000114 ) ;
#11354=CARTESIAN_POINT ( 'NONE',  ( -34.47299999999999898, 12.24483487620000055, -145.0141470300000037 ) ) ;
#11513=( LENGTH_UNIT ( ) NAMED_UNIT ( * ) SI_UNIT ( .MILLI., .METRE. ) );
#11705=ORIENTED_EDGE ( 'NONE', *, *, #10681, .F. ) ;
#11761=VECTOR ( 'NONE', #18851, 1000.000000000000000 ) ;
#11830=AXIS2_PLACEMENT_3D ( 'NONE', #21406, #15802, #19500 ) ;
#11832=VECTOR ( 'NONE', #8561, 1000.000000000000114 ) ;
#11869=ORIENTED_EDGE ( 'NONE', *, *, #18529, .F. ) ;
#11876=FACE_OUTER_BOUND ( 'NONE', #21972, .T. ) ;
#11944=CARTESIAN_POINT ( 'NONE',  ( -26.47299999999999898, 16.00000000000000000, -144.0552959529999839 ) ) ;
#12012=ORIENTED_EDGE ( 'NONE', *, *, #10681, .T. ) ;
#12201=AXIS2_PLACEMENT_3D ( 'NONE', #14600, #12921, #18401 ) ;
#12326=PLANE ( 'NONE',  #1149 ) ;
#12356=ORIENTED_EDGE ( 'NONE', *, *, #14647, .F. ) ;
#12379=AXIS2_PLACEMENT_3D ( 'NONE', #18434, #20109, #3809 ) ;
#12414=CARTESIAN_POINT ( 'NONE',  ( -35.20609992760000040, 16.68710169819999933, -144.5552959529999839 ) ) ;
#12524=CIRCLE ( 'NONE', #1531, 2.000000000000000000 ) ;
#12538=VECTOR ( 'NONE', #5770, 1000.000000000000000 ) ;
#12682=ADVANCED_FACE ( 'NONE', ( #2530 ), #5968, .T. ) ;
#12692=ORIENTED_EDGE ( 'NONE', *, *, #16680, .T. ) ;
#12718=CARTESIAN_POINT ( 'NONE',  ( -34.47299999999999898, 14.00000000000000000, -144.0552959529999839 ) ) ;
#12733=EDGE_CURVE ( 'NONE', #22524, #8477, #2768, .T. ) ;
#12826=CONICAL_SURFACE ( 'NONE', #5981, 2.000000000000003553, 0.7853981633970000820 ) ;
#12921=DIRECTION ( 'NONE',  ( 1.000000000000000000, 2.602084704489999637E-17, -1.701177084980000217E-20 ) ) ;
#12923=( NAMED_UNIT ( * ) PLANE_ANGLE_UNIT ( ) SI_UNIT ( $, .RADIAN. ) );
#12978=VERTEX_POINT ( 'NONE', #13318 ) ;
#13053=B_SPLINE_CURVE_WITH_KNOTS ( 'NONE', 3,
 ( #3939, #17005, #2399, #4290 ),
 .UNSPECIFIED., .F., .F.,
 ( 4, 4 ),
 ( 0.000000000000000000, 0.8059436278830001132 ),
 .UNSPECIFIED. ) ;
#13116=CIRCLE ( 'NONE', #16176, 3.000000000000000888 ) ;
#13255=CYLINDRICAL_SURFACE ( 'NONE', #3049, 2.000000000000003553 ) ;
#13318=CARTESIAN_POINT ( 'NONE',  ( -35.07300000000000040, 11.44852983560000048, -144.5552959529999839 ) ) ;
#13447=DIRECTION ( 'NONE',  ( 1.000000000000000000, 2.602084704489999637E-17, -1.701177084980000217E-20 ) ) ;
#13458=DIRECTION ( 'NONE',  ( 0.000000000000000000, -1.000000000000000000, -2.602084704489999637E-17 ) ) ;
#13577=APPLICATION_CONTEXT ( 'automotive_design' ) ;
#13664=( LENGTH_UNIT ( ) NAMED_UNIT ( * ) SI_UNIT ( .MILLI., .METRE. ) );
#13796=( NAMED_UNIT ( * ) SI_UNIT ( $, .STERADIAN. ) SOLID_ANGLE_UNIT ( ) );
#13823=DIRECTION ( 'NONE',  ( 1.000000000000000000, 2.602084704489999637E-17, -1.701177084980000217E-20 ) ) ;
#13863=FACE_OUTER_BOUND ( 'NONE', #17601, .T. ) ;
#14079=DIRECTION ( 'NONE',  ( 1.000000000000000000, 2.602084704489999637E-17, -1.701177084980000217E-20 ) ) ;
#14082=SHAPE_REPRESENTATION ( 'Slotted Screw', ( #5025 ), #10730 ) ;
#14148=DIRECTION ( 'NONE',  ( -1.000000000000000000, -5.988019148734350335E-18, 1.096099552913726042E-17 ) ) ;
#14180=EDGE_CURVE ( 'NONE', #23345, #23072, #3178, .T. ) ;
#14325=EDGE_CURVE ( 'NONE', #10651, #18413, #15651, .T. ) ;
#14334=CARTESIAN_POINT ( 'NONE',  ( -35.33948162989999986, 16.82262754929999815, -144.5552959529999839 ) ) ;
#14424=CIRCLE ( 'NONE', #16312, 3.000000000000000888 ) ;
#14600=CARTESIAN_POINT ( 'NONE',  ( -35.47299999999999898, 14.00000000000000000, -144.0552959529999839 ) ) ;
#14602=FILL_AREA_STYLE ('',( #21977 ) ) ;
#14647=EDGE_CURVE ( 'NONE', #4899, #18413, #14424, .T. ) ;
#14823=LINE ( 'NONE', #15046, #12538 ) ;
#15000=CARTESIAN_POINT ( 'NONE',  ( -35.47299999999999898, 11.04196010839999964, -143.5552959529999839 ) ) ;
#15046=CARTESIAN_POINT ( 'NONE',  ( -35.07300000000000040, 14.00000000000000000, -144.5552959529999839 ) ) ;
#15097=ORIENTED_EDGE ( 'NONE', *, *, #19785, .F. ) ;
#15304=FACE_OUTER_BOUND ( 'NONE', #21020, .T. ) ;
#15449=( NAMED_UNIT ( * ) PLANE_ANGLE_UNIT ( ) SI_UNIT ( $, .RADIAN. ) );
#15651=B_SPLINE_CURVE_WITH_KNOTS ( 'NONE', 3,
 ( #20821, #10211, #2747, #8435 ),
 .UNSPECIFIED., .F., .F.,
 ( 4, 4 ),
 ( 0.000000000000000000, 0.8059436278830001132 ),
 .UNSPECIFIED. ) ;
#15684=LINE ( 'NONE', #4733, #22715 ) ;
#15766=PLANE ( 'NONE',  #3686 ) ;
#15802=DIRECTION ( 'NONE',  ( 1.000000000000000000, 2.602084704489999637E-17, -1.701177084980000217E-20 ) ) ;
#15814=CARTESIAN_POINT ( 'NONE',  ( -35.33948162989999986, 16.82262754929999815, -143.5552959529999839 ) ) ;
#15926=VERTEX_POINT ( 'NONE', #18949 ) ;
#15945=DIRECTION ( 'NONE',  ( 0.000000000000000000, 1.000000000000000000, 0.000000000000000000 ) ) ;
#15961=ORIENTED_EDGE ( 'NONE', *, *, #10212, .F. ) ;
#15968=CIRCLE ( 'NONE', #7599, 2.600000000000000089 ) ;
#16003=DIRECTION ( 'NONE',  ( -2.602084704489999637E-17, 1.000000000000000000, 0.000000000000000000 ) ) ;
#16176=AXIS2_PLACEMENT_3D ( 'NONE', #736, #13447, #17262 ) ;
#16268=DIRECTION ( 'NONE',  ( 1.000000000000000000, 2.602084704489999637E-17, -1.701177084980000217E-20 ) ) ;
#16307=CARTESIAN_POINT ( 'NONE',  ( -35.47299999999999898, 16.95803989150000035, -143.5552959529999839 ) ) ;
#16312=AXIS2_PLACEMENT_3D ( 'NONE', #16703, #5760, #22186 ) ;
#16534=DIRECTION ( 'NONE',  ( 0.000000000000000000, 1.000000000000000000, 0.000000000000000000 ) ) ;
#16607=( LENGTH_UNIT ( ) NAMED_UNIT ( * ) SI_UNIT ( .MILLI., .METRE. ) );
#16680=EDGE_CURVE ( 'NONE', #15926, #11000, #4373, .T. ) ;
#16690=CIRCLE ( 'NONE', #9063, 2.000000000000000000 ) ;
#16703=CARTESIAN_POINT ( 'NONE',  ( -35.47299999999999898, 14.00000000000000000, -144.0552959529999839 ) ) ;
#16850=SURFACE_SIDE_STYLE ('',( #22095 ) ) ;
#17005=CARTESIAN_POINT ( 'NONE',  ( -35.20609992760000040, 11.31289830180000067, -144.5552959529999839 ) ) ;
#17009=AXIS2_PLACEMENT_3D ( 'NONE', #19760, #9017, #15945 ) ;
#17084=DIRECTION ( 'NONE',  ( 0.000000000000000000, 0.000000000000000000, 1.000000000000000000 ) ) ;
#17145=CARTESIAN_POINT ( 'NONE',  ( -30.97299999999999898, 14.00000000000000000, -144.0552959529999839 ) ) ;
#17210=STYLED_ITEM ( 'NONE', ( #18902 ), #23143 ) ;
#17242=CARTESIAN_POINT ( 'NONE',  ( -34.47299999999999898, 14.00000000000000000, -144.0552959529999839 ) ) ;
#17254=EDGE_CURVE ( 'NONE', #8318, #8477, #13116, .T. ) ;
#17262=DIRECTION ( 'NONE',  ( 0.000000000000000000, 1.000000000000000000, 0.000000000000000000 ) ) ;
#17316=PRODUCT_DEFINITION_CONTEXT ( 'detailed design', #13577, 'design' ) ;
#17317=EDGE_LOOP ( 'NONE', ( #1557, #15961, #11705, #20390 ) ) ;
#17468=CARTESIAN_POINT ( 'NONE',  ( -35.07300000000000040, 16.55147016440000129, -143.5552959529999839 ) ) ;
#17469=ORIENTED_EDGE ( 'NONE', *, *, #20692, .T. ) ;
#17598=( GEOMETRIC_REPRESENTATION_CONTEXT ( 3 ) GLOBAL_UNCERTAINTY_ASSIGNED_CONTEXT ( ( #21378 ) ) GLOBAL_UNIT_ASSIGNED_CONTEXT ( ( #13664, #15449, #13796 ) ) REPRESENTATION_CONTEXT ( 'NONE', 'WORKASPACE' ) );
#17600=FILL_AREA_STYLE ('',( #19253 ) ) ;
#17601=EDGE_LOOP ( 'NONE', ( #7169, #4324 ) ) ;
#17619=ADVANCED_FACE ( 'NONE', ( #3574 ), #18205, .T. ) ;
#17726=VECTOR ( 'NONE', #22033, 1000.000000000000000 ) ;
#17737=DIRECTION ( 'NONE',  ( 0.000000000000000000, 1.000000000000000000, 0.000000000000000000 ) ) ;
#17911=CARTESIAN_POINT ( 'NONE',  ( -35.47299999999999898, 16.95803989150000035, -144.5552959529999839 ) ) ;
#17971=DIRECTION ( 'NONE',  ( -1.000000000000000000, -5.988019148734350335E-18, 1.096099552913726042E-17 ) ) ;
#18089=DIRECTION ( 'NONE',  ( 0.000000000000000000, 0.8775825618903703162, 0.4794255386042076128 ) ) ;
#18171=( GEOMETRIC_REPRESENTATION_CONTEXT ( 3 ) GLOBAL_UNCERTAINTY_ASSIGNED_CONTEXT ( ( #10633 ) ) GLOBAL_UNIT_ASSIGNED_CONTEXT ( ( #16607, #12923, #5896 ) ) REPRESENTATION_CONTEXT ( 'NONE', 'WORKASPACE' ) );
#18205=PLANE ( 'NONE',  #12379 ) ;
#18208=CARTESIAN_POINT ( 'NONE',  ( -34.47299999999999898, 14.00000000000000000, -144.0552959529999839 ) ) ;
#18401=DIRECTION ( 'NONE',  ( -2.602084704489999637E-17, 1.000000000000000000, 0.000000000000000000 ) ) ;
#18413=VERTEX_POINT ( 'NONE', #15000 ) ;
#18422=EDGE_LOOP ( 'NONE', ( #10672, #12692, #2611, #1098 ) ) ;
#18434=CARTESIAN_POINT ( 'NONE',  ( -36.62235836789999865, 14.00000000000000000, -143.5552959529999839 ) ) ;
#18529=EDGE_CURVE ( 'NONE', #18413, #23072, #3832, .T. ) ;
#18561=ORIENTED_EDGE ( 'NONE', *, *, #14325, .T. ) ;
#18597=AXIS2_PLACEMENT_3D ( 'NONE', #22934, #2937, #2710 ) ;
#18756=ORIENTED_EDGE ( 'NONE', *, *, #12733, .T. ) ;
#18851=DIRECTION ( 'NONE',  ( 0.000000000000000000, -1.000000000000000000, 0.000000000000000000 ) ) ;
#18895=CARTESIAN_POINT ( 'NONE',  ( -35.47299999999999898, 11.36725231429999816, -145.4935725690000083 ) ) ;
#18902=PRESENTATION_STYLE_ASSIGNMENT (( #4631 ) ) ;
#18949=CARTESIAN_POINT ( 'NONE',  ( -35.07300000000000040, 16.55147016440000129, -144.5552959529999839 ) ) ;
#18990=ADVANCED_FACE ( 'NONE', ( #13863 ), #15766, .T. ) ;
#19253=FILL_AREA_STYLE_COLOUR ( '', #2405 ) ;
#19324=LINE ( 'NONE', #4932, #11761 ) ;
#19428=EDGE_CURVE ( 'NONE', #8477, #11000, #6731, .T. ) ;
#19500=DIRECTION ( 'NONE',  ( 0.000000000000000000, 1.000000000000000000, 0.000000000000000000 ) ) ;
#19542=EDGE_LOOP ( 'NONE', ( #10662, #913, #5481, #18756, #5576, #10424, #4014, #7323 ) ) ;
#19568=ORIENTED_EDGE ( 'NONE', *, *, #12733, .F. ) ;
#19698=COLOUR_RGB ( '', 0.09019608, 0.27058824, 0.51372549) ;
#19715=ADVANCED_FACE ( 'NONE', ( #131 ), #12826, .T. ) ;
#19717=CIRCLE ( 'NONE', #20482, 2.000000000000000000 ) ;
#19760=CARTESIAN_POINT ( 'NONE',  ( -26.47299999999999898, 14.00000000000000000, -144.0552959529999839 ) ) ;
#19785=EDGE_CURVE ( 'NONE', #7205, #915, #1453, .T. ) ;
#19878=MECHANICAL_DESIGN_GEOMETRIC_PRESENTATION_REPRESENTATION('',(#17210),#17598);
#19884=DIRECTION ( 'NONE',  ( 0.000000000000000000, 1.000000000000000000, 0.000000000000000000 ) ) ;
#20109=DIRECTION ( 'NONE',  ( -1.701177084980000217E-20, 2.602084704489999637E-17, -1.000000000000000000 ) ) ;
#20181=MANIFOLD_SOLID_BREP ( 'lock_assembly.1\\Part1.3\\PartBody', #11059 ) ;
#20390=ORIENTED_EDGE ( 'NONE', *, *, #8927, .F. ) ;
#20482=AXIS2_PLACEMENT_3D ( 'NONE', #1575, #5480, #19884 ) ;
#20503=ORIENTED_EDGE ( 'NONE', *, *, #20826, .T. ) ;
#20692=EDGE_CURVE ( 'NONE', #21589, #4899, #5008, .T. ) ;
#20694=( NAMED_UNIT ( * ) SI_UNIT ( $, .STERADIAN. ) SOLID_ANGLE_UNIT ( ) );
#20794=EDGE_CURVE ( 'NONE', #915, #21589, #8669, .T. ) ;
#20821=CARTESIAN_POINT ( 'NONE',  ( -35.07300000000000040, 11.44852983560000048, -143.5552959529999839 ) ) ;
#20826=EDGE_CURVE ( 'NONE', #21589, #22524, #19717, .T. ) ;
#20830=CARTESIAN_POINT ( 'NONE',  ( -26.47299999999999898, 12.24483487620000055, -145.0141470300000037 ) ) ;
#20939=SURFACE_STYLE_FILL_AREA ( #17600 ) ;
#21020=EDGE_LOOP ( 'NONE', ( #22058, #8225, #9960 ) ) ;
#21255=EDGE_LOOP ( 'NONE', ( #12012, #18561, #8443, #7304 ) ) ;
#21378=UNCERTAINTY_MEASURE_WITH_UNIT (LENGTH_MEASURE( 1.000000000000000082E-05 ), #13664, 'distance_accuracy_value', 'NONE');
#21406=CARTESIAN_POINT ( 'NONE',  ( -35.47299999999999898, 14.00000000000000000, -144.0552959529999839 ) ) ;
#21488=DIRECTION ( 'NONE',  ( -1.000000000000000000, 0.000000000000000000, 0.000000000000000000 ) ) ;
#21589=VERTEX_POINT ( 'NONE', #2898 ) ;
#21651=ORIENTED_EDGE ( 'NONE', *, *, #20826, .F. ) ;
#21972=EDGE_LOOP ( 'NONE', ( #10356, #19568, #21651, #17469, #7485, #9113, #6272, #8894 ) ) ;
#21977=FILL_AREA_STYLE_COLOUR ( '', #19698 ) ;
#22033=DIRECTION ( 'NONE',  ( 0.000000000000000000, 1.000000000000000000, 0.000000000000000000 ) ) ;
#22058=ORIENTED_EDGE ( 'NONE', *, *, #6655, .T. ) ;
#22080=ORIENTED_EDGE ( 'NONE', *, *, #9488, .F. ) ;
#22095=SURFACE_STYLE_FILL_AREA ( #14602 ) ;
#22107=APPLICATION_CONTEXT ( 'automotive_design' ) ;
#22186=DIRECTION ( 'NONE',  ( 0.000000000000000000, 1.000000000000000000, 0.000000000000000000 ) ) ;
#22218=PRODUCT_CONTEXT ( 'NONE', #22107, 'mechanical' ) ;
#22321=ADVANCED_FACE ( 'NONE', ( #7679 ), #7446, .F. ) ;
#22499=ADVANCED_FACE ( 'NONE', ( #15304 ), #23121, .F. ) ;
#22506=CIRCLE ( 'NONE', #11830, 3.000000000000000888 ) ;
#22524=VERTEX_POINT ( 'NONE', #11354 ) ;
#22577=CARTESIAN_POINT ( 'NONE',  ( -35.47299999999999898, 16.95803989150000035, -144.5552959529999839 ) ) ;
#22619=DIRECTION ( 'NONE',  ( 1.000000000000000000, 2.602084704497994558E-17, -1.701177080612860179E-20 ) ) ;
#22715=VECTOR ( 'NONE', #21488, 1000.000000000000000 ) ;
#22927=ADVANCED_FACE ( 'NONE', ( #4413 ), #9871, .T. ) ;
#22934=CARTESIAN_POINT ( 'NONE',  ( -35.07300000000000040, 14.00000000000000000, -144.0552959529999839 ) ) ;
#23072=VERTEX_POINT ( 'NONE', #16307 ) ;
#23121=PLANE ( 'NONE',  #9528 ) ;
#23143=ADVANCED_BREP_SHAPE_REPRESENTATION ( '', ( #20181, #5025 ), #10730 ) ;
#23345=VERTEX_POINT ( 'NONE', #17468 ) ;
#23405=CARTESIAN_POINT ( 'NONE',  ( -35.07300000000000040, 14.00000000000000000, -144.5552959529999839 ) ) ;
#23451=VECTOR ( 'NONE', #3741, 1000.000000000000000 ) ;
#23478=EDGE_CURVE ( 'NONE', #23072, #4899, #22506, .T. ) ;
ENDSEC;
END-ISO-10303-21;
